ISO-10303-21;
HEADER;
/* Generated by software containing ST-Developer
 * from STEP Tools, Inc. (www.steptools.com) 
 */

FILE_DESCRIPTION(
/* description */ ('Lifting hook block with sheave'),
/* implementation_level */ '2;1');

FILE_NAME(
/* name */ 'M16 hook retaining nut.step',
/* time_stamp */ '2026-10-28T03:23:54-07:00',
/* author */ (''),
/* organization */ (''),
/* preprocessor_version */ 'ST-DEVELOPER v20.2',
/* originating_system */ 'Autodesk Translation Framework v15.17.0.0',
/* authorisation */ '');

FILE_SCHEMA (('AUTOMOTIVE_DESIGN { 1 0 10303 214 3 1 1 }'));
ENDSEC;

DATA;
#10=MECHANICAL_DESIGN_GEOMETRIC_PRESENTATION_REPRESENTATION('',(#387),#9391);
#319=SHAPE_REPRESENTATION_RELATIONSHIP('SRR','None',#9553,#349);
#349=ADVANCED_BREP_SHAPE_REPRESENTATION('',(#422),#9388);
#387=STYLED_ITEM('',(#9766),#422);
#422=MANIFOLD_SOLID_BREP('Body1',#4926);
#689=LINE('',#9242,#977);
#690=LINE('',#9247,#978);
#691=LINE('',#9249,#979);
#692=LINE('',#9251,#980);
#693=LINE('',#9252,#981);
#694=LINE('',#9255,#982);
#695=LINE('',#9257,#983);
#696=LINE('',#9258,#984);
#697=LINE('',#9261,#985);
#698=LINE('',#9263,#986);
#699=LINE('',#9264,#987);
#700=LINE('',#9267,#988);
#701=LINE('',#9269,#989);
#702=LINE('',#9270,#990);
#703=LINE('',#9273,#991);
#704=LINE('',#9275,#992);
#705=LINE('',#9276,#993);
#706=LINE('',#9278,#994);
#707=LINE('',#9279,#995);
#977=VECTOR('',#7468,0.7);
#978=VECTOR('',#7473,1.);
#979=VECTOR('',#7474,1.);
#980=VECTOR('',#7475,1.);
#981=VECTOR('',#7476,1.);
#982=VECTOR('',#7479,1.);
#983=VECTOR('',#7480,1.);
#984=VECTOR('',#7481,1.);
#985=VECTOR('',#7484,1.);
#986=VECTOR('',#7485,1.);
#987=VECTOR('',#7486,1.);
#988=VECTOR('',#7489,1.);
#989=VECTOR('',#7490,1.);
#990=VECTOR('',#7491,1.);
#991=VECTOR('',#7494,1.);
#992=VECTOR('',#7495,1.);
#993=VECTOR('',#7496,1.);
#994=VECTOR('',#7499,1.);
#995=VECTOR('',#7500,1.);
#1102=CYLINDRICAL_SURFACE('',#5894,0.7);
#1216=FACE_BOUND('',#1902,.T.);
#1217=FACE_BOUND('',#1904,.T.);
#1496=FACE_OUTER_BOUND('',#1894,.T.);
#1497=FACE_OUTER_BOUND('',#1895,.T.);
#1498=FACE_OUTER_BOUND('',#1896,.T.);
#1499=FACE_OUTER_BOUND('',#1897,.T.);
#1500=FACE_OUTER_BOUND('',#1898,.T.);
#1501=FACE_OUTER_BOUND('',#1899,.T.);
#1502=FACE_OUTER_BOUND('',#1900,.T.);
#1503=FACE_OUTER_BOUND('',#1901,.T.);
#1504=FACE_OUTER_BOUND('',#1903,.T.);
#1894=EDGE_LOOP('',(#4386,#4387,#4388,#4389));
#1895=EDGE_LOOP('',(#4390,#4391,#4392,#4393));
#1896=EDGE_LOOP('',(#4394,#4395,#4396,#4397));
#1897=EDGE_LOOP('',(#4398,#4399,#4400,#4401));
#1898=EDGE_LOOP('',(#4402,#4403,#4404,#4405));
#1899=EDGE_LOOP('',(#4406,#4407,#4408,#4409));
#1900=EDGE_LOOP('',(#4410,#4411,#4412,#4413));
#1901=EDGE_LOOP('',(#4414,#4415,#4416,#4417,#4418,#4419));
#1902=EDGE_LOOP('',(#4420));
#1903=EDGE_LOOP('',(#4421,#4422,#4423,#4424,#4425,#4426));
#1904=EDGE_LOOP('',(#4427));
#2198=CIRCLE('',#5895,0.7);
#2199=CIRCLE('',#5896,0.7);
#2597=VERTEX_POINT('',#9239);
#2598=VERTEX_POINT('',#9241);
#2599=VERTEX_POINT('',#9245);
#2600=VERTEX_POINT('',#9246);
#2601=VERTEX_POINT('',#9248);
#2602=VERTEX_POINT('',#9250);
#2603=VERTEX_POINT('',#9254);
#2604=VERTEX_POINT('',#9256);
#2605=VERTEX_POINT('',#9260);
#2606=VERTEX_POINT('',#9262);
#2607=VERTEX_POINT('',#9266);
#2608=VERTEX_POINT('',#9268);
#2609=VERTEX_POINT('',#9272);
#2610=VERTEX_POINT('',#9274);
#3197=EDGE_CURVE('',#2597,#2597,#2198,.T.);
#3198=EDGE_CURVE('',#2597,#2598,#689,.T.);
#3199=EDGE_CURVE('',#2598,#2598,#2199,.T.);
#3200=EDGE_CURVE('',#2599,#2600,#690,.T.);
#3201=EDGE_CURVE('',#2600,#2601,#691,.T.);
#3202=EDGE_CURVE('',#2602,#2601,#692,.T.);
#3203=EDGE_CURVE('',#2599,#2602,#693,.T.);
#3204=EDGE_CURVE('',#2603,#2599,#694,.T.);
#3205=EDGE_CURVE('',#2604,#2602,#695,.T.);
#3206=EDGE_CURVE('',#2603,#2604,#696,.T.);
#3207=EDGE_CURVE('',#2605,#2603,#697,.T.);
#3208=EDGE_CURVE('',#2606,#2604,#698,.T.);
#3209=EDGE_CURVE('',#2605,#2606,#699,.T.);
#3210=EDGE_CURVE('',#2607,#2605,#700,.T.);
#3211=EDGE_CURVE('',#2608,#2606,#701,.T.);
#3212=EDGE_CURVE('',#2607,#2608,#702,.T.);
#3213=EDGE_CURVE('',#2609,#2607,#703,.T.);
#3214=EDGE_CURVE('',#2610,#2608,#704,.T.);
#3215=EDGE_CURVE('',#2609,#2610,#705,.T.);
#3216=EDGE_CURVE('',#2600,#2609,#706,.T.);
#3217=EDGE_CURVE('',#2601,#2610,#707,.T.);
#4386=ORIENTED_EDGE('',*,*,#3197,.F.);
#4387=ORIENTED_EDGE('',*,*,#3198,.T.);
#4388=ORIENTED_EDGE('',*,*,#3199,.F.);
#4389=ORIENTED_EDGE('',*,*,#3198,.F.);
#4390=ORIENTED_EDGE('',*,*,#3200,.T.);
#4391=ORIENTED_EDGE('',*,*,#3201,.T.);
#4392=ORIENTED_EDGE('',*,*,#3202,.F.);
#4393=ORIENTED_EDGE('',*,*,#3203,.F.);
#4394=ORIENTED_EDGE('',*,*,#3204,.T.);
#4395=ORIENTED_EDGE('',*,*,#3203,.T.);
#4396=ORIENTED_EDGE('',*,*,#3205,.F.);
#4397=ORIENTED_EDGE('',*,*,#3206,.F.);
#4398=ORIENTED_EDGE('',*,*,#3207,.T.);
#4399=ORIENTED_EDGE('',*,*,#3206,.T.);
#4400=ORIENTED_EDGE('',*,*,#3208,.F.);
#4401=ORIENTED_EDGE('',*,*,#3209,.F.);
#4402=ORIENTED_EDGE('',*,*,#3210,.T.);
#4403=ORIENTED_EDGE('',*,*,#3209,.T.);
#4404=ORIENTED_EDGE('',*,*,#3211,.F.);
#4405=ORIENTED_EDGE('',*,*,#3212,.F.);
#4406=ORIENTED_EDGE('',*,*,#3213,.T.);
#4407=ORIENTED_EDGE('',*,*,#3212,.T.);
#4408=ORIENTED_EDGE('',*,*,#3214,.F.);
#4409=ORIENTED_EDGE('',*,*,#3215,.F.);
#4410=ORIENTED_EDGE('',*,*,#3216,.T.);
#4411=ORIENTED_EDGE('',*,*,#3215,.T.);
#4412=ORIENTED_EDGE('',*,*,#3217,.F.);
#4413=ORIENTED_EDGE('',*,*,#3201,.F.);
#4414=ORIENTED_EDGE('',*,*,#3217,.T.);
#4415=ORIENTED_EDGE('',*,*,#3214,.T.);
#4416=ORIENTED_EDGE('',*,*,#3211,.T.);
#4417=ORIENTED_EDGE('',*,*,#3208,.T.);
#4418=ORIENTED_EDGE('',*,*,#3205,.T.);
#4419=ORIENTED_EDGE('',*,*,#3202,.T.);
#4420=ORIENTED_EDGE('',*,*,#3199,.T.);
#4421=ORIENTED_EDGE('',*,*,#3216,.F.);
#4422=ORIENTED_EDGE('',*,*,#3200,.F.);
#4423=ORIENTED_EDGE('',*,*,#3204,.F.);
#4424=ORIENTED_EDGE('',*,*,#3207,.F.);
#4425=ORIENTED_EDGE('',*,*,#3210,.F.);
#4426=ORIENTED_EDGE('',*,*,#3213,.F.);
#4427=ORIENTED_EDGE('',*,*,#3197,.T.);
#4588=PLANE('',#5897);
#4589=PLANE('',#5898);
#4590=PLANE('',#5899);
#4591=PLANE('',#5900);
#4592=PLANE('',#5901);
#4593=PLANE('',#5902);
#4594=PLANE('',#5903);
#4595=PLANE('',#5904);
#4872=ADVANCED_FACE('',(#1496),#1102,.F.);
#4873=ADVANCED_FACE('',(#1497),#4588,.T.);
#4874=ADVANCED_FACE('',(#1498),#4589,.T.);
#4875=ADVANCED_FACE('',(#1499),#4590,.T.);
#4876=ADVANCED_FACE('',(#1500),#4591,.T.);
#4877=ADVANCED_FACE('',(#1501),#4592,.T.);
#4878=ADVANCED_FACE('',(#1502),#4593,.T.);
#4879=ADVANCED_FACE('',(#1503,#1216),#4594,.T.);
#4880=ADVANCED_FACE('',(#1504,#1217),#4595,.F.);
#4926=CLOSED_SHELL('',(#4872,#4873,#4874,#4875,#4876,#4877,#4878,#4879,
#4880));
#5893=AXIS2_PLACEMENT_3D('',#9237,#7462,#7463);
#5894=AXIS2_PLACEMENT_3D('',#9238,#7464,#7465);
#5895=AXIS2_PLACEMENT_3D('',#9240,#7466,#7467);
#5896=AXIS2_PLACEMENT_3D('',#9243,#7469,#7470);
#5897=AXIS2_PLACEMENT_3D('',#9244,#7471,#7472);
#5898=AXIS2_PLACEMENT_3D('',#9253,#7477,#7478);
#5899=AXIS2_PLACEMENT_3D('',#9259,#7482,#7483);
#5900=AXIS2_PLACEMENT_3D('',#9265,#7487,#7488);
#5901=AXIS2_PLACEMENT_3D('',#9271,#7492,#7493);
#5902=AXIS2_PLACEMENT_3D('',#9277,#7497,#7498);
#5903=AXIS2_PLACEMENT_3D('',#9280,#7501,#7502);
#5904=AXIS2_PLACEMENT_3D('',#9281,#7503,#7504);
#7462=DIRECTION('axis',(0.,0.,1.));
#7463=DIRECTION('refdir',(1.,0.,0.));
#7464=DIRECTION('center_axis',(0.,0.,1.));
#7465=DIRECTION('ref_axis',(1.,0.,0.));
#7466=DIRECTION('center_axis',(0.,0.,1.));
#7467=DIRECTION('ref_axis',(1.,0.,0.));
#7468=DIRECTION('',(0.,0.,1.));
#7469=DIRECTION('center_axis',(0.,0.,-1.));
#7470=DIRECTION('ref_axis',(1.,0.,0.));
#7471=DIRECTION('center_axis',(-1.60246890531964E-16,-1.,0.));
#7472=DIRECTION('ref_axis',(1.,-1.60246890531964E-16,0.));
#7473=DIRECTION('',(1.,-1.60246890531964E-16,0.));
#7474=DIRECTION('',(0.,0.,1.));
#7475=DIRECTION('',(1.,-1.60246890531964E-16,0.));
#7476=DIRECTION('',(0.,0.,1.));
#7477=DIRECTION('center_axis',(-0.866025403784439,-0.5,0.));
#7478=DIRECTION('ref_axis',(0.5,-0.866025403784439,0.));
#7479=DIRECTION('',(0.5,-0.866025403784439,0.));
#7480=DIRECTION('',(0.5,-0.866025403784439,0.));
#7481=DIRECTION('',(0.,0.,1.));
#7482=DIRECTION('center_axis',(-0.866025403784439,0.5,0.));
#7483=DIRECTION('ref_axis',(-0.5,-0.866025403784439,0.));
#7484=DIRECTION('',(-0.5,-0.866025403784439,0.));
#7485=DIRECTION('',(-0.5,-0.866025403784439,0.));
#7486=DIRECTION('',(0.,0.,1.));
#7487=DIRECTION('center_axis',(1.60246890531964E-16,1.,0.));
#7488=DIRECTION('ref_axis',(-1.,1.60246890531964E-16,0.));
#7489=DIRECTION('',(-1.,1.60246890531964E-16,0.));
#7490=DIRECTION('',(-1.,1.60246890531964E-16,0.));
#7491=DIRECTION('',(0.,0.,1.));
#7492=DIRECTION('center_axis',(0.866025403784439,0.5,0.));
#7493=DIRECTION('ref_axis',(-0.5,0.866025403784439,0.));
#7494=DIRECTION('',(-0.5,0.866025403784439,0.));
#7495=DIRECTION('',(-0.5,0.866025403784439,0.));
#7496=DIRECTION('',(0.,0.,1.));
#7497=DIRECTION('center_axis',(0.866025403784439,-0.5,0.));
#7498=DIRECTION('ref_axis',(0.5,0.866025403784439,0.));
#7499=DIRECTION('',(0.5,0.866025403784439,0.));
#7500=DIRECTION('',(0.5,0.866025403784439,0.));
#7501=DIRECTION('center_axis',(0.,0.,1.));
#7502=DIRECTION('ref_axis',(1.,0.,0.));
#7503=DIRECTION('center_axis',(0.,0.,1.));
#7504=DIRECTION('ref_axis',(1.,0.,0.));
#9237=CARTESIAN_POINT('',(0.,0.,0.));
#9238=CARTESIAN_POINT('Origin',(0.,0.,5.6));
#9239=CARTESIAN_POINT('',(-0.7,-8.57252759403147E-17,5.7));
#9240=CARTESIAN_POINT('Origin',(0.,0.,5.7));
#9241=CARTESIAN_POINT('',(-0.7,8.57252759403147E-17,6.5));
#9242=CARTESIAN_POINT('',(-0.7,-8.57252759403147E-17,5.6));
#9243=CARTESIAN_POINT('Origin',(0.,0.,6.5));
#9244=CARTESIAN_POINT('Origin',(-0.692820323027552,-1.2,5.7));
#9245=CARTESIAN_POINT('',(-0.692820323027552,-1.2,5.7));
#9246=CARTESIAN_POINT('',(0.692820323027551,-1.2,5.7));
#9247=CARTESIAN_POINT('',(-0.692820323027552,-1.2,5.7));
#9248=CARTESIAN_POINT('',(0.692820323027551,-1.2,6.5));
#9249=CARTESIAN_POINT('',(0.692820323027551,-1.2,5.7));
#9250=CARTESIAN_POINT('',(-0.692820323027552,-1.2,6.5));
#9251=CARTESIAN_POINT('',(-0.692820323027552,-1.2,6.5));
#9252=CARTESIAN_POINT('',(-0.692820323027552,-1.2,5.7));
#9253=CARTESIAN_POINT('Origin',(-1.3856406460551,1.69692038195985E-16,5.7));
#9254=CARTESIAN_POINT('',(-1.3856406460551,1.69692038195985E-16,5.7));
#9255=CARTESIAN_POINT('',(-1.3856406460551,1.69692038195985E-16,5.7));
#9256=CARTESIAN_POINT('',(-1.3856406460551,2.22044604925031E-16,6.5));
#9257=CARTESIAN_POINT('',(-1.3856406460551,1.69692038195985E-16,6.5));
#9258=CARTESIAN_POINT('',(-1.3856406460551,1.69692038195985E-16,5.7));
#9259=CARTESIAN_POINT('Origin',(-0.692820323027551,1.2,5.7));
#9260=CARTESIAN_POINT('',(-0.692820323027551,1.2,5.7));
#9261=CARTESIAN_POINT('',(-0.692820323027551,1.2,5.7));
#9262=CARTESIAN_POINT('',(-0.692820323027551,1.2,6.5));
#9263=CARTESIAN_POINT('',(-0.692820323027551,1.2,6.5));
#9264=CARTESIAN_POINT('',(-0.692820323027551,1.2,5.7));
#9265=CARTESIAN_POINT('Origin',(0.692820323027551,1.2,5.7));
#9266=CARTESIAN_POINT('',(0.692820323027551,1.2,5.7));
#9267=CARTESIAN_POINT('',(0.692820323027551,1.2,5.7));
#9268=CARTESIAN_POINT('',(0.692820323027551,1.2,6.5));
#9269=CARTESIAN_POINT('',(0.692820323027551,1.2,6.5));
#9270=CARTESIAN_POINT('',(0.692820323027551,1.2,5.7));
#9271=CARTESIAN_POINT('Origin',(1.3856406460551,0.,5.7));
#9272=CARTESIAN_POINT('',(1.3856406460551,0.,5.7));
#9273=CARTESIAN_POINT('',(1.3856406460551,0.,5.7));
#9274=CARTESIAN_POINT('',(1.3856406460551,0.,6.5));
#9275=CARTESIAN_POINT('',(1.3856406460551,0.,6.5));
#9276=CARTESIAN_POINT('',(1.3856406460551,0.,5.7));
#9277=CARTESIAN_POINT('Origin',(0.692820323027551,-1.2,5.7));
#9278=CARTESIAN_POINT('',(0.692820323027551,-1.2,5.7));
#9279=CARTESIAN_POINT('',(0.692820323027551,-1.2,6.5));
#9280=CARTESIAN_POINT('Origin',(0.,2.22044604925031E-16,6.5));
#9281=CARTESIAN_POINT('Origin',(0.,2.22044604925031E-16,5.7));
#9351=UNCERTAINTY_MEASURE_WITH_UNIT(LENGTH_MEASURE(0.001),#9392,
'DISTANCE_ACCURACY_VALUE',
'Maximum model space distance between geometric entities at asserted c
onnectivities');
#9354=UNCERTAINTY_MEASURE_WITH_UNIT(LENGTH_MEASURE(0.001),#9392,
'DISTANCE_ACCURACY_VALUE',
'Maximum model space distance between geometric entities at asserted c
onnectivities');
#9388=(
GEOMETRIC_REPRESENTATION_CONTEXT(3)
GLOBAL_UNCERTAINTY_ASSIGNED_CONTEXT((#9351))
GLOBAL_UNIT_ASSIGNED_CONTEXT((#9392,#9394,#9395))
REPRESENTATION_CONTEXT('','3D')
);
#9391=(
GEOMETRIC_REPRESENTATION_CONTEXT(3)
GLOBAL_UNCERTAINTY_ASSIGNED_CONTEXT((#9354))
GLOBAL_UNIT_ASSIGNED_CONTEXT((#9392,#9394,#9395))
REPRESENTATION_CONTEXT('','3D')
);
#9392=(
LENGTH_UNIT()
NAMED_UNIT(*)
SI_UNIT(.CENTI.,.METRE.)
);
#9394=(
NAMED_UNIT(*)
PLANE_ANGLE_UNIT()
SI_UNIT($,.RADIAN.)
);
#9395=(
NAMED_UNIT(*)
SI_UNIT($,.STERADIAN.)
SOLID_ANGLE_UNIT()
);
#9429=SHAPE_DEFINITION_REPRESENTATION(#9509,#9553);
#9509=PRODUCT_DEFINITION_SHAPE('',$,#9590);
#9553=SHAPE_REPRESENTATION('',(#5893),#9388);
#9556=PRODUCT_DEFINITION_CONTEXT('part definition',#9666,'design');
#9590=PRODUCT_DEFINITION('M16 hook retaining nut',
'M16 hook retaining nut',#9626,#9556);
#9626=PRODUCT_DEFINITION_FORMATION('',$,#9701);
#9666=APPLICATION_CONTEXT(
'Core Data for Automotive Mechanical Design Process');
#9667=PRODUCT_CONTEXT('part definition',#9666,'mechanical');
#9701=PRODUCT('M16 hook retaining nut','M16 hook retaining nut',
'M16 hook retaining nut',(#9667));
#9760=COLOUR_RGB('Black',0.12,0.14,0.17);
#9761=FILL_AREA_STYLE_COLOUR('',#9760);
#9762=FILL_AREA_STYLE('',(#9761));
#9763=SURFACE_STYLE_FILL_AREA(#9762);
#9764=SURFACE_SIDE_STYLE('',(#9763));
#9765=SURFACE_STYLE_USAGE(.BOTH.,#9764);
#9766=PRESENTATION_STYLE_ASSIGNMENT((#9765));
ENDSEC;
END-ISO-10303-21;
